ISO-10303-21;
HEADER;
/* Generated by software containing ST-Developer
 * from STEP Tools, Inc. (www.steptools.com) 
 */

FILE_DESCRIPTION(
/* description */ ('Hand-crank flanged shaft unit'),
/* implementation_level */ '2;1');

FILE_NAME(
/* name */ 'Flange bolt sleeve (2).step',
/* time_stamp */ '2026-10-27T18:35:45-07:00',
/* author */ (''),
/* organization */ (''),
/* preprocessor_version */ 'ST-DEVELOPER v20.2',
/* originating_system */ 'Autodesk Translation Framework v15.17.0.0',
/* authorisation */ '');

FILE_SCHEMA (('AUTOMOTIVE_DESIGN { 1 0 10303 214 3 1 1 }'));
ENDSEC;

DATA;
#10=MECHANICAL_DESIGN_GEOMETRIC_PRESENTATION_REPRESENTATION('',(#282),#6805);
#242=SHAPE_REPRESENTATION_RELATIONSHIP('SRR','None',#6903,#262);
#262=ADVANCED_BREP_SHAPE_REPRESENTATION('',(#303),#6786);
#282=STYLED_ITEM('',(#7098),#303);
#303=MANIFOLD_SOLID_BREP('Body1',#3323);
#346=FACE_BOUND('',#766,.T.);
#347=FACE_BOUND('',#768,.T.);
#430=PLANE('',#3626);
#431=PLANE('',#3627);
#549=FACE_OUTER_BOUND('',#763,.T.);
#550=FACE_OUTER_BOUND('',#764,.T.);
#551=FACE_OUTER_BOUND('',#765,.T.);
#552=FACE_OUTER_BOUND('',#767,.T.);
#763=EDGE_LOOP('',(#2407,#2408,#2409,#2410));
#764=EDGE_LOOP('',(#2411,#2412,#2413,#2414));
#765=EDGE_LOOP('',(#2415));
#766=EDGE_LOOP('',(#2416));
#767=EDGE_LOOP('',(#2417));
#768=EDGE_LOOP('',(#2418));
#1031=LINE('',#5106,#1259);
#1032=LINE('',#5112,#1260);
#1259=VECTOR('',#4126,0.425);
#1260=VECTOR('',#4133,0.595);
#1465=CIRCLE('',#3621,0.425);
#1466=CIRCLE('',#3622,0.425);
#1467=CIRCLE('',#3624,0.595);
#1468=CIRCLE('',#3625,0.595);
#1621=VERTEX_POINT('',#5103);
#1622=VERTEX_POINT('',#5105);
#1623=VERTEX_POINT('',#5109);
#1624=VERTEX_POINT('',#5111);
#1921=EDGE_CURVE('',#1621,#1621,#1465,.T.);
#1922=EDGE_CURVE('',#1621,#1622,#1031,.T.);
#1923=EDGE_CURVE('',#1622,#1622,#1466,.T.);
#1924=EDGE_CURVE('',#1623,#1623,#1467,.T.);
#1925=EDGE_CURVE('',#1623,#1624,#1032,.T.);
#1926=EDGE_CURVE('',#1624,#1624,#1468,.T.);
#2407=ORIENTED_EDGE('',*,*,#1921,.F.);
#2408=ORIENTED_EDGE('',*,*,#1922,.T.);
#2409=ORIENTED_EDGE('',*,*,#1923,.T.);
#2410=ORIENTED_EDGE('',*,*,#1922,.F.);
#2411=ORIENTED_EDGE('',*,*,#1924,.F.);
#2412=ORIENTED_EDGE('',*,*,#1925,.T.);
#2413=ORIENTED_EDGE('',*,*,#1926,.T.);
#2414=ORIENTED_EDGE('',*,*,#1925,.F.);
#2415=ORIENTED_EDGE('',*,*,#1924,.T.);
#2416=ORIENTED_EDGE('',*,*,#1921,.T.);
#2417=ORIENTED_EDGE('',*,*,#1926,.F.);
#2418=ORIENTED_EDGE('',*,*,#1923,.F.);
#3081=CYLINDRICAL_SURFACE('',#3620,0.425);
#3082=CYLINDRICAL_SURFACE('',#3623,0.595);
#3166=ADVANCED_FACE('',(#549),#3081,.F.);
#3167=ADVANCED_FACE('',(#550),#3082,.T.);
#3168=ADVANCED_FACE('',(#551,#346),#430,.T.);
#3169=ADVANCED_FACE('',(#552,#347),#431,.F.);
#3323=CLOSED_SHELL('',(#3166,#3167,#3168,#3169));
#3619=AXIS2_PLACEMENT_3D('',#5101,#4120,#4121);
#3620=AXIS2_PLACEMENT_3D('',#5102,#4122,#4123);
#3621=AXIS2_PLACEMENT_3D('',#5104,#4124,#4125);
#3622=AXIS2_PLACEMENT_3D('',#5107,#4127,#4128);
#3623=AXIS2_PLACEMENT_3D('',#5108,#4129,#4130);
#3624=AXIS2_PLACEMENT_3D('',#5110,#4131,#4132);
#3625=AXIS2_PLACEMENT_3D('',#5113,#4134,#4135);
#3626=AXIS2_PLACEMENT_3D('',#5114,#4136,#4137);
#3627=AXIS2_PLACEMENT_3D('',#5115,#4138,#4139);
#4120=DIRECTION('axis',(0.,0.,1.));
#4121=DIRECTION('refdir',(1.,0.,0.));
#4122=DIRECTION('center_axis',(0.,1.,0.));
#4123=DIRECTION('ref_axis',(1.,0.,0.));
#4124=DIRECTION('center_axis',(0.,-1.,0.));
#4125=DIRECTION('ref_axis',(1.,0.,0.));
#4126=DIRECTION('',(0.,-1.,0.));
#4127=DIRECTION('center_axis',(0.,-1.,0.));
#4128=DIRECTION('ref_axis',(1.,0.,0.));
#4129=DIRECTION('center_axis',(0.,1.,0.));
#4130=DIRECTION('ref_axis',(1.,0.,0.));
#4131=DIRECTION('center_axis',(0.,1.,0.));
#4132=DIRECTION('ref_axis',(1.,0.,0.));
#4133=DIRECTION('',(0.,-1.,0.));
#4134=DIRECTION('center_axis',(0.,1.,0.));
#4135=DIRECTION('ref_axis',(1.,0.,0.));
#4136=DIRECTION('center_axis',(0.,1.,0.));
#4137=DIRECTION('ref_axis',(1.,0.,0.));
#4138=DIRECTION('center_axis',(0.,1.,0.));
#4139=DIRECTION('ref_axis',(1.,0.,0.));
#5101=CARTESIAN_POINT('',(0.,0.,0.));
#5102=CARTESIAN_POINT('Origin',(3.2,-1.,4.3));
#5103=CARTESIAN_POINT('',(2.775,0.,4.3));
#5104=CARTESIAN_POINT('Origin',(3.2,0.,4.3));
#5105=CARTESIAN_POINT('',(2.775,-1.,4.3));
#5106=CARTESIAN_POINT('',(2.775,-1.,4.3));
#5107=CARTESIAN_POINT('Origin',(3.2,-1.,4.3));
#5108=CARTESIAN_POINT('Origin',(3.2,-1.,4.3));
#5109=CARTESIAN_POINT('',(2.605,0.,4.3));
#5110=CARTESIAN_POINT('Origin',(3.2,0.,4.3));
#5111=CARTESIAN_POINT('',(2.605,-1.,4.3));
#5112=CARTESIAN_POINT('',(2.605,-1.,4.3));
#5113=CARTESIAN_POINT('Origin',(3.2,-1.,4.3));
#5114=CARTESIAN_POINT('Origin',(3.2,0.,4.3));
#5115=CARTESIAN_POINT('Origin',(3.2,-1.,4.3));
#6761=UNCERTAINTY_MEASURE_WITH_UNIT(LENGTH_MEASURE(0.001),#6806,
'DISTANCE_ACCURACY_VALUE',
'Maximum model space distance between geometric entities at asserted c
onnectivities');
#6780=UNCERTAINTY_MEASURE_WITH_UNIT(LENGTH_MEASURE(0.001),#6806,
'DISTANCE_ACCURACY_VALUE',
'Maximum model space distance between geometric entities at asserted c
onnectivities');
#6786=(
GEOMETRIC_REPRESENTATION_CONTEXT(3)
GLOBAL_UNCERTAINTY_ASSIGNED_CONTEXT((#6761))
GLOBAL_UNIT_ASSIGNED_CONTEXT((#6806,#6808,#6809))
REPRESENTATION_CONTEXT('','3D')
);
#6805=(
GEOMETRIC_REPRESENTATION_CONTEXT(3)
GLOBAL_UNCERTAINTY_ASSIGNED_CONTEXT((#6780))
GLOBAL_UNIT_ASSIGNED_CONTEXT((#6806,#6808,#6809))
REPRESENTATION_CONTEXT('','3D')
);
#6806=(
LENGTH_UNIT()
NAMED_UNIT(*)
SI_UNIT(.CENTI.,.METRE.)
);
#6808=(
NAMED_UNIT(*)
PLANE_ANGLE_UNIT()
SI_UNIT($,.RADIAN.)
);
#6809=(
NAMED_UNIT(*)
SI_UNIT($,.STERADIAN.)
SOLID_ANGLE_UNIT()
);
#6815=SHAPE_DEFINITION_REPRESENTATION(#6839,#6903);
#6839=PRODUCT_DEFINITION_SHAPE('',$,#6928);
#6903=SHAPE_REPRESENTATION('',(#3619),#6786);
#6922=PRODUCT_DEFINITION_CONTEXT('part definition',#6996,'design');
#6928=PRODUCT_DEFINITION('Flange bolt sleeve (2)',
'Flange bolt sleeve (2)',#6952,#6922);
#6952=PRODUCT_DEFINITION_FORMATION('',$,#7003);
#6996=APPLICATION_CONTEXT(
'Core Data for Automotive Mechanical Design Process');
#6997=PRODUCT_CONTEXT('part definition',#6996,'mechanical');
#7003=PRODUCT('Flange bolt sleeve (2)','Flange bolt sleeve (2)',
'Flange bolt sleeve (2)',(#6997));
#7092=COLOUR_RGB('Black',0.12,0.14,0.17);
#7093=FILL_AREA_STYLE_COLOUR('',#7092);
#7094=FILL_AREA_STYLE('',(#7093));
#7095=SURFACE_STYLE_FILL_AREA(#7094);
#7096=SURFACE_SIDE_STYLE('',(#7095));
#7097=SURFACE_STYLE_USAGE(.BOTH.,#7096);
#7098=PRESENTATION_STYLE_ASSIGNMENT((#7097));
ENDSEC;
END-ISO-10303-21;
